ISO-10303-21;
HEADER;
FILE_DESCRIPTION (('STEP AP203'),
    '1' );
FILE_NAME ('1602p_c_17.step',
    '2026-10-31T14:11:27',
    ( '' ),
    ( '' ),
    'SwSTEP 2.0',
    'SolidWorks 2024',
    '' );
FILE_SCHEMA (( 'AUTOMOTIVE_DESIGN' ));
ENDSEC;

DATA;
#8=CARTESIAN_POINT ( 'NONE',  ( -14.54830929633810044, -2.787889851644860251, 8.000000000004460432 ) ) ;
#20=AXIS2_PLACEMENT_3D ( 'NONE', #1988, #305, #1861 ) ;
#46=CARTESIAN_POINT ( 'NONE',  ( -14.70588235717489844, 25.77561860482770228, 6.750000000004400036 ) ) ;
#66=DIRECTION ( 'NONE',  ( -1.138590270679730064E-14, -2.220446049251245514E-15, -1.000000000000000000 ) ) ;
#107=ORIENTED_EDGE ( 'NONE', *, *, #9525, .T. ) ;
#111=CARTESIAN_POINT ( 'NONE',  ( -14.00000000144730095, -4.350228928435719844, 8.000000000004460432 ) ) ;
#159=CARTESIAN_POINT ( 'NONE',  ( -14.00000000000000000, -19.99999999944489915, 5.500000000004489742 ) ) ;
#213=CARTESIAN_POINT ( 'NONE',  ( -14.70588235717489844, 25.77561860482770228, 5.500000000004400036 ) ) ;
#229=CYLINDRICAL_SURFACE ( 'NONE', #3934, 2.500000000000000000 ) ;
#269=SHAPE_REPRESENTATION_RELATIONSHIP ( 'NONE' , 'NONE' ,  #488, #12210 ) ;
#279=CARTESIAN_POINT ( 'NONE',  ( -22.52506283708569867, 28.95208917575130414, 8.000000000004481748 ) ) ;
#305=DIRECTION ( 'NONE',  ( -1.138590270679734009E-14, -2.220446049251240387E-15, -1.000000000000000000 ) ) ;
#380=CARTESIAN_POINT ( 'NONE',  ( -14.98746859791960162, 26.70208920133150343, 8.000000000004400036 ) ) ;
#415=DIRECTION ( 'NONE',  ( 1.000000000000000000, 0.000000000000000000, 0.000000000000000000 ) ) ;
#474=DIRECTION ( 'NONE',  ( -1.138590270679734009E-14, -2.220446049251240387E-15, -1.000000000000000000 ) ) ;
#479=AXIS2_PLACEMENT_3D ( 'NONE', #2013, #5569, #16719 ) ;
#482=CIRCLE ( 'NONE', #15677, 2.499999999999998668 ) ;
#488=SHAPE_REPRESENTATION ( '1602p_c_17', ( #12739 ), #13514 ) ;
#514=DIRECTION ( 'NONE',  ( 1.138590270679730064E-14, 2.220446049251240387E-15, 1.000000000000000000 ) ) ;
#529=EDGE_CURVE ( 'NONE', #10876, #12306, #23421, .T. ) ;
#635=DIRECTION ( 'NONE',  ( 1.138590270679730064E-14, 2.220446049251235259E-15, 1.000000000000000000 ) ) ;
#666=LINE ( 'NONE', #4365, #15048 ) ;
#695=VECTOR ( 'NONE', #13903, 1000.000000000000000 ) ;
#709=EDGE_CURVE ( 'NONE', #4115, #1299, #12822, .T. ) ;
#723=EDGE_LOOP ( 'NONE', ( #14438, #13051, #6044, #8193, #9529, #11889, #19904, #12108, #1672, #3809, #15184, #2137, #14325, #14667 ) ) ;
#740=EDGE_CURVE ( 'NONE', #9811, #6317, #14408, .T. ) ;
#744=AXIS2_PLACEMENT_3D ( 'NONE', #21021, #1047, #4747 ) ;
#745=CARTESIAN_POINT ( 'NONE',  ( -22.50000000000000000, -20.00000001665527805, 5.500000000004588330 ) ) ;
#772=ORIENTED_EDGE ( 'NONE', *, *, #11755, .F. ) ;
#799=EDGE_LOOP ( 'NONE', ( #7526, #13181 ) ) ;
#845=DIRECTION ( 'NONE',  ( 1.138590270679734009E-14, 2.220446049251240387E-15, 1.000000000000000000 ) ) ;
#905=DIRECTION ( 'NONE',  ( 1.138590270679728013E-14, 2.220446049251240387E-15, 1.000000000000000000 ) ) ;
#916=ORIENTED_EDGE ( 'NONE', *, *, #3595, .T. ) ;
#1028=AXIS2_PLACEMENT_3D ( 'NONE', #21199, #4821, #19313 ) ;
#1047=DIRECTION ( 'NONE',  ( 2.528178268246854219E-29, 2.220446049251370154E-15, 1.000000000000000000 ) ) ;
#1056=ADVANCED_FACE ( 'NONE', ( #12193 ), #10419, .T. ) ;
#1064=CARTESIAN_POINT ( 'NONE',  ( -17.47493719149670000, 26.45208920939580111, 6.750000000004429346 ) ) ;
#1131=DIRECTION ( 'NONE',  ( 2.528178268246854219E-29, 2.220446049251370154E-15, 1.000000000000000000 ) ) ;
#1156=DIRECTION ( 'NONE',  ( 1.138590270679734009E-14, 2.220446049251240387E-15, 1.000000000000000000 ) ) ;
#1157=DIRECTION ( 'NONE',  ( -1.138590270679730064E-14, -2.220446049251230526E-15, -1.000000000000000000 ) ) ;
#1160=CIRCLE ( 'NONE', #4209, 2.500000000000000000 ) ;
#1178=VECTOR ( 'NONE', #2952, 1000.000000000000000 ) ;
#1251=CARTESIAN_POINT ( 'NONE',  ( -20.00000000000000000, -20.00000000000000000, 8.000000000004559908 ) ) ;
#1279=MANIFOLD_SOLID_BREP ( 'Imported1', #3817 ) ;
#1295=FACE_BOUND ( 'NONE', #13599, .T. ) ;
#1299=VERTEX_POINT ( 'NONE', #380 ) ;
#1428=DIRECTION ( 'NONE',  ( -1.000000000000000000, -6.662111140531837817E-09, 1.144917494144693313E-14 ) ) ;
#1672=ORIENTED_EDGE ( 'NONE', *, *, #13792, .F. ) ;
#1775=VERTEX_POINT ( 'NONE', #22207 ) ;
#1783=VERTEX_POINT ( 'NONE', #7505 ) ;
#1791=VECTOR ( 'NONE', #11198, 1000.000000000000000 ) ;
#1838=ADVANCED_FACE ( 'NONE', ( #4639 ), #4517, .F. ) ;
#1861=DIRECTION ( 'NONE',  ( -1.000000000000000000, -6.662111140531837817E-09, 1.110223024625157172E-14 ) ) ;
#1942=CIRCLE ( 'NONE', #11476, 2.500000000000001332 ) ;
#1951=DIRECTION ( 'NONE',  ( -1.138590270679734009E-14, -2.220446049251240387E-15, -1.000000000000000000 ) ) ;
#1988=CARTESIAN_POINT ( 'NONE',  ( -20.00000000397270128, 22.95208919257349933, 8.000000000004460432 ) ) ;
#1998=ORIENTED_EDGE ( 'NONE', *, *, #6028, .F. ) ;
#2013=CARTESIAN_POINT ( 'NONE',  ( -22.52506283708579815, 28.95208917575130414, 6.750000000004479972 ) ) ;
#2099=CYLINDRICAL_SURFACE ( 'NONE', #8210, 2.500000000000000000 ) ;
#2137=ORIENTED_EDGE ( 'NONE', *, *, #10292, .F. ) ;
#2142=APPLICATION_CONTEXT ( 'configuration controlled 3d designs of mechanical parts and assemblies' ) ;
#2158=VECTOR ( 'NONE', #19665, 1000.000000000000000 ) ;
#2175=VECTOR ( 'NONE', #7146, 1000.000000000000000 ) ;
#2295=AXIS2_PLACEMENT_3D ( 'NONE', #1064, #8454, #14021 ) ;
#2350=ORIENTED_EDGE ( 'NONE', *, *, #3124, .F. ) ;
#2427=EDGE_CURVE ( 'NONE', #1783, #13768, #6680, .T. ) ;
#2434=CARTESIAN_POINT ( 'NONE',  ( -17.50000000397270128, 22.95208920922877738, 5.500000000004431122 ) ) ;
#2489=CARTESIAN_POINT ( 'NONE',  ( -20.00000000397270128, 22.95208919257349933, 6.750000000004470202 ) ) ;
#2516=ORIENTED_EDGE ( 'NONE', *, *, #4438, .T. ) ;
#2569=CARTESIAN_POINT ( 'NONE',  ( 0.000000000000000000, 0.000000000000000000, 0.000000000000000000 ) ) ;
#2694=EDGE_CURVE ( 'NONE', #6087, #1299, #14053, .T. ) ;
#2714=CARTESIAN_POINT ( 'NONE',  ( -22.52506282043049879, 26.45208917575140006, 8.000000000004488854 ) ) ;
#2738=ORIENTED_EDGE ( 'NONE', *, *, #11377, .F. ) ;
#2830=EDGE_LOOP ( 'NONE', ( #772, #16239, #7465, #14594 ) ) ;
#2843=LINE ( 'NONE', #21577, #13161 ) ;
#2847=LINE ( 'NONE', #17335, #4489 ) ;
#2946=AXIS2_PLACEMENT_3D ( 'NONE', #18008, #11003, #12880 ) ;
#2951=AXIS2_PLACEMENT_3D ( 'NONE', #19793, #7212, #3639 ) ;
#2952=DIRECTION ( 'NONE',  ( 1.138590270679730064E-14, 2.220446049251240387E-15, 1.000000000000000000 ) ) ;
#3070=CARTESIAN_POINT ( 'NONE',  ( -16.50000000202540207, 1.899127378699219992, 8.000000000004471090 ) ) ;
#3098=DIRECTION ( 'NONE',  ( 1.138590270679734009E-14, 2.220446049251240387E-15, 1.000000000000000000 ) ) ;
#3102=FACE_OUTER_BOUND ( 'NONE', #2830, .T. ) ;
#3124=EDGE_CURVE ( 'NONE', #4115, #10804, #2843, .T. ) ;
#3215=ORIENTED_EDGE ( 'NONE', *, *, #13792, .T. ) ;
#3237=EDGE_CURVE ( 'NONE', #22084, #11858, #4052, .T. ) ;
#3247=EDGE_LOOP ( 'NONE', ( #13344, #13513, #21944, #8145 ) ) ;
#3250=AXIS2_PLACEMENT_3D ( 'NONE', #5428, #17790, #21566 ) ;
#3283=ORIENTED_EDGE ( 'NONE', *, *, #529, .F. ) ;
#3334=LINE ( 'NONE', #14613, #2175 ) ;
#3395=EDGE_CURVE ( 'NONE', #8919, #21873, #11057, .T. ) ;
#3492=PRODUCT_DEFINITION_FORMATION_WITH_SPECIFIED_SOURCE ( 'ANY', '', #19920, .NOT_KNOWN. ) ;
#3581=ORIENTED_EDGE ( 'NONE', *, *, #16600, .T. ) ;
#3595=EDGE_CURVE ( 'NONE', #6087, #10804, #1160, .T. ) ;
#3639=DIRECTION ( 'NONE',  ( -1.000000000000000000, -9.259433497721235207E-11, 1.142026288351377283E-14 ) ) ;
#3655=AXIS2_PLACEMENT_3D ( 'NONE', #6189, #474, #7736 ) ;
#3674=VERTEX_POINT ( 'NONE', #14086 ) ;
#3723=ORIENTED_EDGE ( 'NONE', *, *, #11766, .T. ) ;
#3734=ADVANCED_FACE ( 'NONE', ( #20983, #19204, #6988 ), #14211, .T. ) ;
#3756=ORIENTED_EDGE ( 'NONE', *, *, #12062, .T. ) ;
#3768=VERTEX_POINT ( 'NONE', #279 ) ;
#3777=PLANE ( 'NONE',  #479 ) ;
#3796=FACE_OUTER_BOUND ( 'NONE', #12905, .T. ) ;
#3809=ORIENTED_EDGE ( 'NONE', *, *, #6903, .F. ) ;
#3817=CLOSED_SHELL ( 'NONE', ( #17794, #8801, #17519, #16080, #5260, #9800, #21567, #15125, #13592, #6474, #17276, #5500, #12196, #15882, #23372, #19874, #1838, #1056, #7912, #3734 ) ) ;
#3934=AXIS2_PLACEMENT_3D ( 'NONE', #7500, #14731, #21961 ) ;
#3999=AXIS2_PLACEMENT_3D ( 'NONE', #2714, #66, #7447 ) ;
#4028=VECTOR ( 'NONE', #20942, 1000.000000000000000 ) ;
#4039=VERTEX_POINT ( 'NONE', #745 ) ;
#4052=CIRCLE ( 'NONE', #17329, 2.500000000000000000 ) ;
#4061=VECTOR ( 'NONE', #12054, 1000.000000000000000 ) ;
#4090=AXIS2_PLACEMENT_3D ( 'NONE', #18249, #13028, #9585 ) ;
#4106=DIRECTION ( 'NONE',  ( -1.138590270679730064E-14, -2.220446049251240387E-15, -1.000000000000000000 ) ) ;
#4110=CARTESIAN_POINT ( 'NONE',  ( -22.50000000000000000, -20.00000001665527805, 6.750000000004588330 ) ) ;
#4115=VERTEX_POINT ( 'NONE', #17156 ) ;
#4145=DIRECTION ( 'NONE',  ( -1.000000000000000000, -6.662111466122900240E-09, 1.138590272159020020E-14 ) ) ;
#4209=AXIS2_PLACEMENT_3D ( 'NONE', #22525, #905, #6493 ) ;
#4297=CARTESIAN_POINT ( 'NONE',  ( -27.50000000434249969, 26.95208919188020147, 6.750000000004539480 ) ) ;
#4332=DIRECTION ( 'NONE',  ( -1.138590270679730064E-14, -2.220446049251235259E-15, -1.000000000000000000 ) ) ;
#4365=CARTESIAN_POINT ( 'NONE',  ( -26.00000000397269773, 22.95208919201850151, 8.000000000004529710 ) ) ;
#4384=EDGE_CURVE ( 'NONE', #3768, #4115, #12521, .T. ) ;
#4408=AXIS2_PLACEMENT_3D ( 'NONE', #4297, #6540, #8206 ) ;
#4426=ORIENTED_EDGE ( 'NONE', *, *, #3595, .F. ) ;
#4429=LINE ( 'NONE', #11699, #15906 ) ;
#4438=EDGE_CURVE ( 'NONE', #12469, #15535, #19815, .T. ) ;
#4484=ORIENTED_EDGE ( 'NONE', *, *, #13660, .T. ) ;
#4489=VECTOR ( 'NONE', #8553, 1000.000000000000000 ) ;
#4501=CARTESIAN_POINT ( 'NONE',  ( -14.00000000397270128, 22.95208919312850071, 5.500000000004400036 ) ) ;
#4508=FACE_BOUND ( 'NONE', #4799, .T. ) ;
#4517=CYLINDRICAL_SURFACE ( 'NONE', #4408, 2.500000000000002220 ) ;
#4534=ORIENTED_EDGE ( 'NONE', *, *, #15298, .T. ) ;
#4564=FACE_OUTER_BOUND ( 'NONE', #16918, .T. ) ;
#4639=FACE_OUTER_BOUND ( 'NONE', #22424, .T. ) ;
#4747=DIRECTION ( 'NONE',  ( 1.000000000000000000, -1.138590270679730064E-14, 4.484155085839414876E-45 ) ) ;
#4770=CARTESIAN_POINT ( 'NONE',  ( -20.00000000397270128, 22.95208919257349933, 8.000000000004460432 ) ) ;
#4799=EDGE_LOOP ( 'NONE', ( #3723, #5665 ) ) ;
#4821=DIRECTION ( 'NONE',  ( 1.000000000000000000, -1.053113628799951803E-24, -1.138589415207818163E-14 ) ) ;
#4855=LINE ( 'NONE', #6402, #17384 ) ;
#4857=EDGE_CURVE ( 'NONE', #19671, #3674, #9868, .T. ) ;
#4937=AXIS2_PLACEMENT_3D ( 'NONE', #16307, #8967, #7301 ) ;
#4996=ORIENTED_EDGE ( 'NONE', *, *, #21881, .T. ) ;
#5127=ORIENTED_EDGE ( 'NONE', *, *, #8767, .T. ) ;
#5131=ORIENTED_EDGE ( 'NONE', *, *, #10292, .T. ) ;
#5132=ORIENTED_EDGE ( 'NONE', *, *, #15395, .T. ) ;
#5143=DIRECTION ( 'NONE',  ( -0.8823529412199648814, 0.4705882352125658197, 9.020562075079400046E-15 ) ) ;
#5144=DIRECTION ( 'NONE',  ( -9.248890187689720549E-11, 1.000000000000000000, -2.220446048198180498E-15 ) ) ;
#5168=FACE_OUTER_BOUND ( 'NONE', #6993, .T. ) ;
#5179=ORIENTED_EDGE ( 'NONE', *, *, #4857, .F. ) ;
#5215=DIRECTION ( 'NONE',  ( 1.138590270679730064E-14, 2.220446049251235259E-15, 1.000000000000000000 ) ) ;
#5260=ADVANCED_FACE ( 'NONE', ( #4508, #1295, #17340 ), #11904, .F. ) ;
#5306=AXIS2_PLACEMENT_3D ( 'NONE', #10607, #5352, #7264 ) ;
#5344=ORIENTED_EDGE ( 'NONE', *, *, #14514, .T. ) ;
#5347=DIRECTION ( 'NONE',  ( 1.138590270679734009E-14, 2.220446049251240387E-15, 1.000000000000000000 ) ) ;
#5352=DIRECTION ( 'NONE',  ( 1.138590270679730064E-14, 2.220446049251230526E-15, 1.000000000000000000 ) ) ;
#5428=CARTESIAN_POINT ( 'NONE',  ( -26.00000000000000000, -20.00000000055539928, 6.750000000004630074 ) ) ;
#5439=FACE_OUTER_BOUND ( 'NONE', #3247, .T. ) ;
#5483=SHAPE_DEFINITION_REPRESENTATION ( #6421, #488 ) ;
#5500=ADVANCED_FACE ( 'NONE', ( #4564 ), #18945, .T. ) ;
#5545=DIRECTION ( 'NONE',  ( 1.138590270679731958E-14, 2.220446049251245514E-15, 1.000000000000000000 ) ) ;
#5556=ORIENTED_EDGE ( 'NONE', *, *, #11755, .T. ) ;
#5569=DIRECTION ( 'NONE',  ( -6.662111466122901068E-09, 1.000000000000000000, -2.220445973397092972E-15 ) ) ;
#5607=CARTESIAN_POINT ( 'NONE',  ( -14.00000000000000000, -19.99999999944489915, 5.500000000004489742 ) ) ;
#5664=DIRECTION ( 'NONE',  ( -9.249283497051789705E-11, 1.000000000000000000, -2.220446048198130405E-15 ) ) ;
#5665=ORIENTED_EDGE ( 'NONE', *, *, #15228, .T. ) ;
#5713=ORIENTED_EDGE ( 'NONE', *, *, #18190, .F. ) ;
#5734=ORIENTED_EDGE ( 'NONE', *, *, #21739, .T. ) ;
#5801=AXIS2_PLACEMENT_3D ( 'NONE', #7240, #5215, #7020 ) ;
#5828=DIRECTION ( 'NONE',  ( 1.138590270679734009E-14, 2.220446049251240387E-15, 1.000000000000000000 ) ) ;
#5861=CARTESIAN_POINT ( 'NONE',  ( -14.98746859791960162, 26.70208920133150343, 5.500000000004400036 ) ) ;
#5870=( NAMED_UNIT ( * ) PLANE_ANGLE_UNIT ( ) SI_UNIT ( $, .RADIAN. ) );
#5934=DIRECTION ( 'NONE',  ( -1.000000000000000000, -6.662111140531837817E-09, 1.144917494144693313E-14 ) ) ;
#5955=ORIENTED_EDGE ( 'NONE', *, *, #15228, .F. ) ;
#5980=VECTOR ( 'NONE', #9832, 1000.000000000000000 ) ;
#5994=AXIS2_PLACEMENT_3D ( 'NONE', #10220, #13645, #22658 ) ;
#5995=CYLINDRICAL_SURFACE ( 'NONE', #6597, 2.500000000000000444 ) ;
#6028=EDGE_CURVE ( 'NONE', #10063, #23388, #12511, .T. ) ;
#6031=CARTESIAN_POINT ( 'NONE',  ( -20.00000000397270128, 22.95208919257349933, 6.750000000004470202 ) ) ;
#6044=ORIENTED_EDGE ( 'NONE', *, *, #23294, .F. ) ;
#6045=FACE_OUTER_BOUND ( 'NONE', #7125, .T. ) ;
#6087=VERTEX_POINT ( 'NONE', #5861 ) ;
#6089=DIRECTION ( 'NONE',  ( -0.8823529412199648814, 0.4705882352125658197, 9.020562075079400046E-15 ) ) ;
#6109=DIRECTION ( 'NONE',  ( 9.248855984704951398E-11, -1.000000000000000000, 2.220446048198180498E-15 ) ) ;
#6112=ORIENTED_EDGE ( 'NONE', *, *, #529, .T. ) ;
#6147=CYLINDRICAL_SURFACE ( 'NONE', #8050, 5.999999999999999112 ) ;
#6148=ORIENTED_EDGE ( 'NONE', *, *, #6903, .T. ) ;
#6152=EDGE_CURVE ( 'NONE', #10876, #6317, #4429, .T. ) ;
#6169=LINE ( 'NONE', #15415, #14464 ) ;
#6189=CARTESIAN_POINT ( 'NONE',  ( -20.00000000000000000, -20.00000000000000000, 8.000000000004559908 ) ) ;
#6206=ORIENTED_EDGE ( 'NONE', *, *, #21447, .F. ) ;
#6261=CARTESIAN_POINT ( 'NONE',  ( -25.01253141238650102, 26.70208918381559826, 5.500000000004510170 ) ) ;
#6317=VERTEX_POINT ( 'NONE', #22938 ) ;
#6325=DIRECTION ( 'NONE',  ( 1.138590270679730064E-14, 2.220446049251240387E-15, 1.000000000000000000 ) ) ;
#6389=AXIS2_PLACEMENT_3D ( 'NONE', #10303, #17415, #15747 ) ;
#6402=CARTESIAN_POINT ( 'NONE',  ( -25.29411765129259848, 25.77561860384869874, 6.750000000004519940 ) ) ;
#6421=PRODUCT_DEFINITION_SHAPE ( 'NONE', 'NONE',  #16907 ) ;
#6474=ADVANCED_FACE ( 'NONE', ( #3796 ), #229, .T. ) ;
#6493=DIRECTION ( 'NONE',  ( 0.9949874374308178560, 0.09999999677427207079, -1.144917494144692682E-14 ) ) ;
#6520=DIRECTION ( 'NONE',  ( 0.9949874374308235181, 0.09999999677421511635, -1.179611963664228193E-14 ) ) ;
#6540=DIRECTION ( 'NONE',  ( 1.138590270679730064E-14, 2.220446049251240387E-15, 1.000000000000000000 ) ) ;
#6597=AXIS2_PLACEMENT_3D ( 'NONE', #15571, #635, #8461 ) ;
#6602=ORIENTED_EDGE ( 'NONE', *, *, #14795, .T. ) ;
#6680=CIRCLE ( 'NONE', #10485, 6.000000000000000000 ) ;
#6682=LINE ( 'NONE', #11364, #15693 ) ;
#6747=ORIENTED_EDGE ( 'NONE', *, *, #22321, .T. ) ;
#6759=AXIS2_PLACEMENT_3D ( 'NONE', #22867, #10189, #9950 ) ;
#6903=EDGE_CURVE ( 'NONE', #11858, #12809, #13006, .T. ) ;
#6910=VERTEX_POINT ( 'NONE', #20047 ) ;
#6945=CARTESIAN_POINT ( 'NONE',  ( -27.50000000434249969, 26.95208919188020147, 8.000000000004540368 ) ) ;
#6988=FACE_OUTER_BOUND ( 'NONE', #723, .T. ) ;
#6993=EDGE_LOOP ( 'NONE', ( #5955, #5556, #6206, #16271 ) ) ;
#7005=EDGE_LOOP ( 'NONE', ( #19255, #15398, #6112, #6747 ) ) ;
#7020=DIRECTION ( 'NONE',  ( 0.7806762821592939661, -0.6249356306644248127, -7.632783294297949638E-15 ) ) ;
#7039=ORIENTED_EDGE ( 'NONE', *, *, #13073, .F. ) ;
#7084=CIRCLE ( 'NONE', #13900, 6.000000000000000000 ) ;
#7125=EDGE_LOOP ( 'NONE', ( #19003, #18968, #22936, #18839 ) ) ;
#7133=AXIS2_PLACEMENT_3D ( 'NONE', #17018, #4332, #11600 ) ;
#7146=DIRECTION ( 'NONE',  ( 9.248890187689720549E-11, -1.000000000000000000, 2.220446048198180498E-15 ) ) ;
#7212=DIRECTION ( 'NONE',  ( 1.138590270679730064E-14, 2.220446049251240387E-15, 1.000000000000000000 ) ) ;
#7226=EDGE_LOOP ( 'NONE', ( #9275, #11663, #916, #2350 ) ) ;
#7240=CARTESIAN_POINT ( 'NONE',  ( -12.59661859122890171, -1.225550774622820027, 8.000000000004430234 ) ) ;
#7264=DIRECTION ( 'NONE',  ( 0.7806762821593211665, -0.6249356306643909509, -7.632783294297951215E-15 ) ) ;
#7293=UNCERTAINTY_MEASURE_WITH_UNIT (LENGTH_MEASURE( 1.000000000000000082E-05 ), #20115, 'distance_accuracy_value', 'NONE');
#7301=DIRECTION ( 'NONE',  ( -6.662111140531837817E-09, 1.000000000000000000, -2.081668171172169697E-15 ) ) ;
#7410=ORIENTED_EDGE ( 'NONE', *, *, #14795, .F. ) ;
#7411=CARTESIAN_POINT ( 'NONE',  ( -17.47493720815189633, 28.95208920939580111, 8.000000000004419576 ) ) ;
#7419=ORIENTED_EDGE ( 'NONE', *, *, #22588, .F. ) ;
#7447=DIRECTION ( 'NONE',  ( -6.662111140531837817E-09, 1.000000000000000000, -2.081668171172169697E-15 ) ) ;
#7465=ORIENTED_EDGE ( 'NONE', *, *, #11879, .T. ) ;
#7500=CARTESIAN_POINT ( 'NONE',  ( -16.50000000202540207, 1.899127378699219992, 6.750000000004470202 ) ) ;
#7505=CARTESIAN_POINT ( 'NONE',  ( -14.70588235717489844, 25.77561860482770228, 8.000000000004400036 ) ) ;
#7526=ORIENTED_EDGE ( 'NONE', *, *, #11377, .T. ) ;
#7570=CARTESIAN_POINT ( 'NONE',  ( -12.50000000434259917, 26.95208919326709918, 6.750000000004369838 ) ) ;
#7670=EDGE_CURVE ( 'NONE', #15793, #19671, #22881, .T. ) ;
#7682=AXIS2_PLACEMENT_3D ( 'NONE', #18451, #9893, #20335 ) ;
#7727=ORIENTED_EDGE ( 'NONE', *, *, #16600, .F. ) ;
#7736=DIRECTION ( 'NONE',  ( -1.000000000000000000, -6.662111140531837817E-09, 1.110223024625157172E-14 ) ) ;
#7737=AXIS2_PLACEMENT_3D ( 'NONE', #10537, #15974, #15507 ) ;
#7895=CIRCLE ( 'NONE', #5994, 2.499999999999998668 ) ;
#7912=ADVANCED_FACE ( 'NONE', ( #9140 ), #3777, .T. ) ;
#7948=AXIS2_PLACEMENT_3D ( 'NONE', #17011, #7999, #6089 ) ;
#7999=DIRECTION ( 'NONE',  ( -1.138590270679730064E-14, -2.220446049251240387E-15, -1.000000000000000000 ) ) ;
#8020=VECTOR ( 'NONE', #10540, 1000.000000000000000 ) ;
#8050=AXIS2_PLACEMENT_3D ( 'NONE', #6031, #10085, #22757 ) ;
#8103=AXIS2_PLACEMENT_3D ( 'NONE', #14318, #18364, #20129 ) ;
#8131=LINE ( 'NONE', #15117, #4061 ) ;
#8145=ORIENTED_EDGE ( 'NONE', *, *, #2694, .T. ) ;
#8191=CARTESIAN_POINT ( 'NONE',  ( -20.00000000397270128, 22.95208919257349933, 6.750000000004470202 ) ) ;
#8193=ORIENTED_EDGE ( 'NONE', *, *, #9525, .F. ) ;
#8206=DIRECTION ( 'NONE',  ( -0.8823529412199652144, 0.4705882352125652091, 9.020562075079389002E-15 ) ) ;
#8210=AXIS2_PLACEMENT_3D ( 'NONE', #7570, #5545, #12802 ) ;
#8214=CYLINDRICAL_SURFACE ( 'NONE', #2295, 2.500000000000000000 ) ;
#8215=LINE ( 'NONE', #19258, #12800 ) ;
#8262=AXIS2_PLACEMENT_3D ( 'NONE', #1251, #21086, #15509 ) ;
#8288=ORIENTED_EDGE ( 'NONE', *, *, #4384, .T. ) ;
#8310=ORIENTED_EDGE ( 'NONE', *, *, #14344, .F. ) ;
#8398=DIRECTION ( 'NONE',  ( 1.000000000000000000, -1.138590270679730064E-14, 4.484155085839414876E-45 ) ) ;
#8447=VECTOR ( 'NONE', #19755, 1000.000000000000000 ) ;
#8454=DIRECTION ( 'NONE',  ( 1.138590270679728013E-14, 2.220446049251240387E-15, 1.000000000000000000 ) ) ;
#8461=DIRECTION ( 'NONE',  ( 0.7806762821592939661, -0.6249356306644248127, -7.632783294297949638E-15 ) ) ;
#8523=DIRECTION ( 'NONE',  ( 1.138590270679730064E-14, 2.220446049251245514E-15, 1.000000000000000000 ) ) ;
#8553=DIRECTION ( 'NONE',  ( 1.138590270679734009E-14, 2.220446049251240387E-15, 1.000000000000000000 ) ) ;
#8575=CARTESIAN_POINT ( 'NONE',  ( -22.50000000000000000, -20.00000001665527805, 8.000000000004588330 ) ) ;
#8582=ORIENTED_EDGE ( 'NONE', *, *, #15181, .F. ) ;
#8716=CARTESIAN_POINT ( 'NONE',  ( -14.54830929633820169, -2.787889851644860251, 5.500000000004459544 ) ) ;
#8767=EDGE_CURVE ( 'NONE', #16965, #10063, #14178, .T. ) ;
#8801=ADVANCED_FACE ( 'NONE', ( #5168 ), #10072, .F. ) ;
#8919=VERTEX_POINT ( 'NONE', #14775 ) ;
#8967=DIRECTION ( 'NONE',  ( 1.138590270679730064E-14, 2.220446049251245514E-15, 1.000000000000000000 ) ) ;
#8976=CARTESIAN_POINT ( 'NONE',  ( -14.00000000397270128, 22.95208919312850071, 8.000000000004400036 ) ) ;
#9018=VERTEX_POINT ( 'NONE', #19775 ) ;
#9109=PLANE ( 'NONE',  #3250 ) ;
#9120=CARTESIAN_POINT ( 'NONE',  ( -20.00000000397270128, 22.95208919257349933, 5.500000000004459544 ) ) ;
#9140=FACE_OUTER_BOUND ( 'NONE', #9872, .T. ) ;
#9163=VECTOR ( 'NONE', #4145, 1000.000000000000000 ) ;
#9250=CARTESIAN_POINT ( 'NONE',  ( -14.00000000202540029, 1.899127378930369980, 5.500000000004440004 ) ) ;
#9275=ORIENTED_EDGE ( 'NONE', *, *, #709, .T. ) ;
#9310=ORIENTED_EDGE ( 'NONE', *, *, #21447, .T. ) ;
#9315=( NAMED_UNIT ( * ) SI_UNIT ( $, .STERADIAN. ) SOLID_ANGLE_UNIT ( ) );
#9364=ORIENTED_EDGE ( 'NONE', *, *, #22486, .F. ) ;
#9374=VECTOR ( 'NONE', #14863, 1000.000000000000000 ) ;
#9525=EDGE_CURVE ( 'NONE', #17339, #11032, #18985, .T. ) ;
#9529=ORIENTED_EDGE ( 'NONE', *, *, #22715, .F. ) ;
#9585=DIRECTION ( 'NONE',  ( 0.9949874374308178560, 0.09999999677427207079, -1.179611963664228824E-14 ) ) ;
#9604=ORIENTED_EDGE ( 'NONE', *, *, #13073, .T. ) ;
#9652=EDGE_LOOP ( 'NONE', ( #5131, #7419, #16388, #23357 ) ) ;
#9707=DIRECTION ( 'NONE',  ( 1.138590270679730064E-14, 2.220446049251240387E-15, 1.000000000000000000 ) ) ;
#9763=VERTEX_POINT ( 'NONE', #8575 ) ;
#9796=CIRCLE ( 'NONE', #8262, 2.499999999999998668 ) ;
#9800=ADVANCED_FACE ( 'NONE', ( #10244 ), #8214, .T. ) ;
#9811=VERTEX_POINT ( 'NONE', #15445 ) ;
#9832=DIRECTION ( 'NONE',  ( 1.138590270679730064E-14, 2.220446049251240387E-15, 1.000000000000000000 ) ) ;
#9846=ORIENTED_EDGE ( 'NONE', *, *, #3124, .T. ) ;
#9859=DIRECTION ( 'NONE',  ( -1.000000000000000000, -6.662111140531837817E-09, 1.144917494144693313E-14 ) ) ;
#9868=CIRCLE ( 'NONE', #5306, 2.500000000000000000 ) ;
#9872=EDGE_LOOP ( 'NONE', ( #8288, #9846, #12578, #19432 ) ) ;
#9893=DIRECTION ( 'NONE',  ( 1.138590270679734009E-14, 2.220446049251240387E-15, 1.000000000000000000 ) ) ;
#9950=DIRECTION ( 'NONE',  ( 0.000000000000000000, 1.000000000000000000, -9.248890187689720549E-11 ) ) ;
#9991=CARTESIAN_POINT ( 'NONE',  ( -20.00000000000000000, -20.00000000000000000, 5.500000000004559020 ) ) ;
#9996=LINE ( 'NONE', #4110, #10565 ) ;
#10063=VERTEX_POINT ( 'NONE', #6261 ) ;
#10072=CYLINDRICAL_SURFACE ( 'NONE', #7737, 2.499999999999998668 ) ;
#10085=DIRECTION ( 'NONE',  ( 1.138590270679730064E-14, 2.220446049251235259E-15, 1.000000000000000000 ) ) ;
#10106=DIRECTION ( 'NONE',  ( -1.000000000000000000, -6.662111140531837817E-09, 1.144917494144693313E-14 ) ) ;
#10134=FACE_OUTER_BOUND ( 'NONE', #11493, .T. ) ;
#10145=VECTOR ( 'NONE', #5144, 1000.000000000000000 ) ;
#10181=CARTESIAN_POINT ( 'NONE',  ( -14.00000000202540029, 1.899127378930379972, 8.000000000004439116 ) ) ;
#10189=DIRECTION ( 'NONE',  ( 1.000000000000000000, -1.053068847079585977E-24, -1.138589415280572122E-14 ) ) ;
#10202=ORIENTED_EDGE ( 'NONE', *, *, #23294, .T. ) ;
#10220=CARTESIAN_POINT ( 'NONE',  ( -20.00000000000000000, -20.00000000000000000, 5.500000000004559020 ) ) ;
#10244=FACE_OUTER_BOUND ( 'NONE', #7226, .T. ) ;
#10292=EDGE_CURVE ( 'NONE', #13768, #22084, #12211, .T. ) ;
#10303=CARTESIAN_POINT ( 'NONE',  ( -16.50000000144740042, -4.350228928666989958, 5.500000000004489742 ) ) ;
#10325=ORIENTED_EDGE ( 'NONE', *, *, #3237, .T. ) ;
#10408=CYLINDRICAL_SURFACE ( 'NONE', #17906, 6.000000000000109246 ) ;
#10419=CYLINDRICAL_SURFACE ( 'NONE', #4937, 2.499999999999998668 ) ;
#10421=CARTESIAN_POINT ( 'NONE',  ( -14.00000000000000000, -19.99999999944489915, 6.750000000004490630 ) ) ;
#10440=LINE ( 'NONE', #21329, #2158 ) ;
#10485=AXIS2_PLACEMENT_3D ( 'NONE', #16212, #1951, #19778 ) ;
#10514=DIRECTION ( 'NONE',  ( -1.000000000000000000, -9.259433497721235207E-11, 1.142026288351377283E-14 ) ) ;
#10537=CARTESIAN_POINT ( 'NONE',  ( -20.00000000000000000, -20.00000000000000000, 6.750000000004559908 ) ) ;
#10540=DIRECTION ( 'NONE',  ( 9.249283497051789705E-11, -1.000000000000000000, 2.220446048198130405E-15 ) ) ;
#10565=VECTOR ( 'NONE', #15384, 1000.000000000000000 ) ;
#10574=DIRECTION ( 'NONE',  ( -1.138590270679730064E-14, -2.220446049251240387E-15, -1.000000000000000000 ) ) ;
#10584=ORIENTED_EDGE ( 'NONE', *, *, #4438, .F. ) ;
#10592=CARTESIAN_POINT ( 'NONE',  ( -12.59661859122890171, -1.225550774622830019, 5.500000000004429346 ) ) ;
#10607=CARTESIAN_POINT ( 'NONE',  ( -16.50000000202540207, 1.899127378699210000, 5.500000000004470202 ) ) ;
#10666=EDGE_LOOP ( 'NONE', ( #5734, #12988, #17964, #14723 ) ) ;
#10694=CARTESIAN_POINT ( 'NONE',  ( -22.52506283708579815, 28.95208917575130414, 5.500000000004479972 ) ) ;
#10802=CARTESIAN_POINT ( 'NONE',  ( -25.29411765129259848, 25.77561860384869874, 5.500000000004519940 ) ) ;
#10804=VERTEX_POINT ( 'NONE', #17747 ) ;
#10876=VERTEX_POINT ( 'NONE', #11094 ) ;
#11003=DIRECTION ( 'NONE',  ( -1.138590270679730064E-14, -2.220446049251240387E-15, -1.000000000000000000 ) ) ;
#11032=VERTEX_POINT ( 'NONE', #17987 ) ;
#11057=CIRCLE ( 'NONE', #20, 2.499999999999998668 ) ;
#11094=CARTESIAN_POINT ( 'NONE',  ( -26.00000000000000000, -20.00000000055539928, 5.500000000004630074 ) ) ;
#11175=LINE ( 'NONE', #9250, #19870 ) ;
#11198=DIRECTION ( 'NONE',  ( 1.138590270679730064E-14, 2.220446049251240387E-15, 1.000000000000000000 ) ) ;
#11264=CIRCLE ( 'NONE', #3655, 2.499999999999998668 ) ;
#11321=CIRCLE ( 'NONE', #7133, 5.999999999999999112 ) ;
#11364=CARTESIAN_POINT ( 'NONE',  ( -26.00000000397269773, 22.95208919201850151, 5.500000000004529710 ) ) ;
#11374=DIRECTION ( 'NONE',  ( -1.000000000000000000, -9.259433497721235207E-11, 1.127570259384904101E-14 ) ) ;
#11377=EDGE_CURVE ( 'NONE', #21873, #8919, #20013, .T. ) ;
#11435=APPLICATION_CONTEXT ( 'configuration controlled 3d designs of mechanical parts and assemblies' ) ;
#11437=EDGE_CURVE ( 'NONE', #16515, #9811, #3334, .T. ) ;
#11460=CIRCLE ( 'NONE', #17126, 2.499999999999998668 ) ;
#11476=AXIS2_PLACEMENT_3D ( 'NONE', #17441, #18996, #6520 ) ;
#11493=EDGE_LOOP ( 'NONE', ( #6148, #15979, #18386, #4534 ) ) ;
#11555=CARTESIAN_POINT ( 'NONE',  ( -20.00000000397270128, 22.95208919257349933, 5.500000000004459544 ) ) ;
#11600=DIRECTION ( 'NONE',  ( -0.8823529412199823119, 0.4705882352125332901, 8.962737959213505425E-15 ) ) ;
#11620=EDGE_CURVE ( 'NONE', #9018, #16515, #18537, .T. ) ;
#11663=ORIENTED_EDGE ( 'NONE', *, *, #2694, .F. ) ;
#11692=CYLINDRICAL_SURFACE ( 'NONE', #7682, 2.499999999999998668 ) ;
#11699=CARTESIAN_POINT ( 'NONE',  ( -26.00000000000000000, -20.00000000055539928, 6.750000000004630074 ) ) ;
#11745=DIRECTION ( 'NONE',  ( -9.248855984704951398E-11, 1.000000000000000000, -2.220446048198180498E-15 ) ) ;
#11755=EDGE_CURVE ( 'NONE', #12528, #1775, #2847, .T. ) ;
#11766=EDGE_CURVE ( 'NONE', #4039, #12528, #7895, .T. ) ;
#11833=EDGE_CURVE ( 'NONE', #23388, #17339, #4855, .T. ) ;
#11858=VERTEX_POINT ( 'NONE', #15315 ) ;
#11869=VERTEX_POINT ( 'NONE', #4501 ) ;
#11879=EDGE_CURVE ( 'NONE', #4039, #9763, #9996, .T. ) ;
#11889=ORIENTED_EDGE ( 'NONE', *, *, #21739, .F. ) ;
#11900=DIRECTION ( 'NONE',  ( 1.138590270679730064E-14, 2.220446049251240387E-15, 1.000000000000000000 ) ) ;
#11904=PLANE ( 'NONE',  #744 ) ;
#11979=PLANE ( 'NONE',  #1028 ) ;
#11991=FACE_OUTER_BOUND ( 'NONE', #19812, .T. ) ;
#12035=DIRECTION ( 'NONE',  ( -1.138590270679734009E-14, -2.220446049251240387E-15, -1.000000000000000000 ) ) ;
#12054=DIRECTION ( 'NONE',  ( 1.138590270679730064E-14, 2.220446049251240387E-15, 1.000000000000000000 ) ) ;
#12062=EDGE_CURVE ( 'NONE', #9018, #15793, #15095, .T. ) ;
#12095=DESIGN_CONTEXT ( 'detailed design', #11435, 'design' ) ;
#12108=ORIENTED_EDGE ( 'NONE', *, *, #11437, .F. ) ;
#12193=FACE_OUTER_BOUND ( 'NONE', #15068, .T. ) ;
#12196=ADVANCED_FACE ( 'NONE', ( #19310 ), #19425, .T. ) ;
#12210=ADVANCED_BREP_SHAPE_REPRESENTATION ( '', ( #1279, #12739 ), #13514 ) ;
#12211=LINE ( 'NONE', #15753, #8020 ) ;
#12230=CARTESIAN_POINT ( 'NONE',  ( -12.50000000434259917, 26.95208919326709918, 5.500000000004369838 ) ) ;
#12281=ORIENTED_EDGE ( 'NONE', *, *, #17073, .T. ) ;
#12306=VERTEX_POINT ( 'NONE', #159 ) ;
#12469=VERTEX_POINT ( 'NONE', #2434 ) ;
#12482=DIRECTION ( 'NONE',  ( 0.7806762821592939661, -0.6249356306644248127, -7.632783294297949638E-15 ) ) ;
#12500=CARTESIAN_POINT ( 'NONE',  ( -14.54830929662709949, 0.3367883020382380632, 5.500000000004449774 ) ) ;
#12511=CIRCLE ( 'NONE', #7948, 2.499999999999999112 ) ;
#12521=LINE ( 'NONE', #7411, #8447 ) ;
#12528=VERTEX_POINT ( 'NONE', #13121 ) ;
#12578=ORIENTED_EDGE ( 'NONE', *, *, #15181, .T. ) ;
#12739=AXIS2_PLACEMENT_3D ( 'NONE', #2569, #13380, #415 ) ;
#12799=VECTOR ( 'NONE', #23322, 1000.000000000000000 ) ;
#12800=VECTOR ( 'NONE', #3098, 1000.000000000000000 ) ;
#12802=DIRECTION ( 'NONE',  ( 0.9949874374308235181, 0.09999999677421517186, -1.144917494144692682E-14 ) ) ;
#12809=VERTEX_POINT ( 'NONE', #8 ) ;
#12822=CIRCLE ( 'NONE', #4090, 2.500000000000000000 ) ;
#12869=ORIENTED_EDGE ( 'NONE', *, *, #22715, .T. ) ;
#12880=DIRECTION ( 'NONE',  ( 1.000000000000000000, 9.250447630115842075E-11, -1.110223024625156383E-14 ) ) ;
#12905=EDGE_LOOP ( 'NONE', ( #10325, #22774, #16950, #16127 ) ) ;
#12988=ORIENTED_EDGE ( 'NONE', *, *, #15395, .F. ) ;
#13006=CIRCLE ( 'NONE', #5801, 2.500000000000000444 ) ;
#13028=DIRECTION ( 'NONE',  ( -1.138590270679728013E-14, -2.220446049251240387E-15, -1.000000000000000000 ) ) ;
#13051=ORIENTED_EDGE ( 'NONE', *, *, #4384, .F. ) ;
#13073=EDGE_CURVE ( 'NONE', #12469, #8919, #15441, .T. ) ;
#13121=CARTESIAN_POINT ( 'NONE',  ( -17.50000000000000000, -19.99999998334472195, 5.500000000004530598 ) ) ;
#13151=LINE ( 'NONE', #22388, #5980 ) ;
#13161=VECTOR ( 'NONE', #10574, 1000.000000000000000 ) ;
#13181=ORIENTED_EDGE ( 'NONE', *, *, #3395, .T. ) ;
#13221=CARTESIAN_POINT ( 'NONE',  ( -20.00000000397270128, 22.95208919257349933, 5.500000000004459544 ) ) ;
#13296=LINE ( 'NONE', #20420, #9163 ) ;
#13344=ORIENTED_EDGE ( 'NONE', *, *, #15363, .T. ) ;
#13380=DIRECTION ( 'NONE',  ( 0.000000000000000000, 0.000000000000000000, 1.000000000000000000 ) ) ;
#13423=DIRECTION ( 'NONE',  ( 1.138590270679730064E-14, 2.220446049251240387E-15, 1.000000000000000000 ) ) ;
#13464=ORIENTED_EDGE ( 'NONE', *, *, #17073, .F. ) ;
#13513=ORIENTED_EDGE ( 'NONE', *, *, #17234, .F. ) ;
#13514=( GEOMETRIC_REPRESENTATION_CONTEXT ( 3 ) GLOBAL_UNCERTAINTY_ASSIGNED_CONTEXT ( ( #7293 ) ) GLOBAL_UNIT_ASSIGNED_CONTEXT ( ( #20115, #5870, #9315 ) ) REPRESENTATION_CONTEXT ( 'NONE', 'WORKASPACE' ) );
#13562=EDGE_CURVE ( 'NONE', #11869, #13768, #13151, .T. ) ;
#13592=ADVANCED_FACE ( 'NONE', ( #17768 ), #11979, .T. ) ;
#13599=EDGE_LOOP ( 'NONE', ( #3581, #2516 ) ) ;
#13645=DIRECTION ( 'NONE',  ( 1.138590270679734009E-14, 2.220446049251240387E-15, 1.000000000000000000 ) ) ;
#13646=CYLINDRICAL_SURFACE ( 'NONE', #19125, 2.499999999999998668 ) ;
#13660=EDGE_CURVE ( 'NONE', #1775, #9763, #9796, .T. ) ;
#13768=VERTEX_POINT ( 'NONE', #8976 ) ;
#13792=EDGE_CURVE ( 'NONE', #12809, #16515, #18502, .T. ) ;
#13879=LINE ( 'NONE', #19227, #1178 ) ;
#13900=AXIS2_PLACEMENT_3D ( 'NONE', #9120, #14692, #16353 ) ;
#13903=DIRECTION ( 'NONE',  ( 1.138590270679734009E-14, 2.220446049251240387E-15, 1.000000000000000000 ) ) ;
#14021=DIRECTION ( 'NONE',  ( 0.9949874374308178560, 0.09999999677427207079, -1.144917494144692682E-14 ) ) ;
#14053=LINE ( 'NONE', #21174, #4028 ) ;
#14086=CARTESIAN_POINT ( 'NONE',  ( -14.00000000202540029, 1.899127378930369980, 5.500000000004440004 ) ) ;
#14174=DIRECTION ( 'NONE',  ( 1.138590270679730064E-14, 2.220446049251240387E-15, 1.000000000000000000 ) ) ;
#14178=CIRCLE ( 'NONE', #17219, 2.499999999999998668 ) ;
#14211=PLANE ( 'NONE',  #22776 ) ;
#14318=CARTESIAN_POINT ( 'NONE',  ( -20.00000000397270128, 22.95208919257349933, 5.500000000004459544 ) ) ;
#14325=ORIENTED_EDGE ( 'NONE', *, *, #2427, .F. ) ;
#14344=EDGE_CURVE ( 'NONE', #12306, #9018, #23302, .T. ) ;
#14377=AXIS2_PLACEMENT_3D ( 'NONE', #19070, #9707, #18734 ) ;
#14408=CIRCLE ( 'NONE', #21968, 6.000000000000109246 ) ;
#14438=ORIENTED_EDGE ( 'NONE', *, *, #709, .F. ) ;
#14464=VECTOR ( 'NONE', #13423, 1000.000000000000000 ) ;
#14514=EDGE_CURVE ( 'NONE', #15793, #12809, #22332, .T. ) ;
#14594=ORIENTED_EDGE ( 'NONE', *, *, #13660, .F. ) ;
#14609=ORIENTED_EDGE ( 'NONE', *, *, #11620, .F. ) ;
#14613=CARTESIAN_POINT ( 'NONE',  ( -14.00000000000000000, -19.99999999944489915, 8.000000000004488854 ) ) ;
#14614=CIRCLE ( 'NONE', #19922, 2.500000000000001332 ) ;
#14655=LINE ( 'NONE', #22001, #21889 ) ;
#14667=ORIENTED_EDGE ( 'NONE', *, *, #15363, .F. ) ;
#14692=DIRECTION ( 'NONE',  ( 1.138590270679734009E-14, 2.220446049251240387E-15, 1.000000000000000000 ) ) ;
#14702=ORIENTED_EDGE ( 'NONE', *, *, #8767, .F. ) ;
#14723=ORIENTED_EDGE ( 'NONE', *, *, #6152, .T. ) ;
#14731=DIRECTION ( 'NONE',  ( 1.138590270679731958E-14, 2.220446049251235259E-15, 1.000000000000000000 ) ) ;
#14775=CARTESIAN_POINT ( 'NONE',  ( -17.50000000397270128, 22.95208920922877738, 8.000000000004432010 ) ) ;
#14795=EDGE_CURVE ( 'NONE', #15535, #21873, #8215, .T. ) ;
#14863=DIRECTION ( 'NONE',  ( 1.138590270679730064E-14, 2.220446049251240387E-15, 1.000000000000000000 ) ) ;
#14870=EDGE_LOOP ( 'NONE', ( #14702, #8582, #4426, #19818, #14916, #5713, #5179, #21641, #19599, #8310, #3283, #15112, #13464, #1998 ) ) ;
#14916=ORIENTED_EDGE ( 'NONE', *, *, #21539, .F. ) ;
#14985=FACE_OUTER_BOUND ( 'NONE', #20752, .T. ) ;
#15046=VERTEX_POINT ( 'NONE', #213 ) ;
#15048=VECTOR ( 'NONE', #11745, 1000.000000000000000 ) ;
#15068=EDGE_LOOP ( 'NONE', ( #10202, #9364, #5127, #4996 ) ) ;
#15074=CARTESIAN_POINT ( 'NONE',  ( -14.00000000144740042, -4.350228928435730502, 6.750000000004459544 ) ) ;
#15095=CIRCLE ( 'NONE', #6389, 2.500000000000000444 ) ;
#15112=ORIENTED_EDGE ( 'NONE', *, *, #17372, .F. ) ;
#15117=CARTESIAN_POINT ( 'NONE',  ( -14.00000000202540029, 1.899127378930379972, 6.750000000004440004 ) ) ;
#15125=ADVANCED_FACE ( 'NONE', ( #6045 ), #18533, .T. ) ;
#15181=EDGE_CURVE ( 'NONE', #10804, #16965, #13296, .T. ) ;
#15184=ORIENTED_EDGE ( 'NONE', *, *, #3237, .F. ) ;
#15228=EDGE_CURVE ( 'NONE', #12528, #4039, #11460, .T. ) ;
#15281=ORIENTED_EDGE ( 'NONE', *, *, #11620, .T. ) ;
#15298=EDGE_CURVE ( 'NONE', #19671, #11858, #13879, .T. ) ;
#15315=CARTESIAN_POINT ( 'NONE',  ( -14.54830929662709949, 0.3367883020382470560, 8.000000000004449774 ) ) ;
#15345=DIRECTION ( 'NONE',  ( -1.000000000000000000, -6.662111140531837817E-09, 1.144917494144693313E-14 ) ) ;
#15363=EDGE_CURVE ( 'NONE', #1299, #1783, #1942, .T. ) ;
#15384=DIRECTION ( 'NONE',  ( 1.138590270679734009E-14, 2.220446049251240387E-15, 1.000000000000000000 ) ) ;
#15395=EDGE_CURVE ( 'NONE', #6910, #23250, #6169, .T. ) ;
#15398=ORIENTED_EDGE ( 'NONE', *, *, #6152, .F. ) ;
#15415=CARTESIAN_POINT ( 'NONE',  ( -26.00000000397269773, 22.95208919201850151, 6.750000000004529710 ) ) ;
#15421=DIRECTION ( 'NONE',  ( 1.138590270679734009E-14, 2.220446049251240387E-15, 1.000000000000000000 ) ) ;
#15441=LINE ( 'NONE', #22675, #695 ) ;
#15445=CARTESIAN_POINT ( 'NONE',  ( -14.00000000000000000, -19.99999999944489915, 8.000000000004488854 ) ) ;
#15507=DIRECTION ( 'NONE',  ( -1.000000000000000000, -6.662111140531837817E-09, 1.144917494144693313E-14 ) ) ;
#15509=DIRECTION ( 'NONE',  ( -1.000000000000000000, -6.662111140531837817E-09, 1.110223024625157172E-14 ) ) ;
#15535=VERTEX_POINT ( 'NONE', #23355 ) ;
#15571=CARTESIAN_POINT ( 'NONE',  ( -12.59661859122890171, -1.225550774622820027, 6.750000000004429346 ) ) ;
#15677=AXIS2_PLACEMENT_3D ( 'NONE', #11555, #5828, #5934 ) ;
#15693=VECTOR ( 'NONE', #6109, 1000.000000000000000 ) ;
#15725=FACE_OUTER_BOUND ( 'NONE', #7005, .T. ) ;
#15747=DIRECTION ( 'NONE',  ( 1.000000000000000000, 9.250447630115842075E-11, -1.144917494144692525E-14 ) ) ;
#15753=CARTESIAN_POINT ( 'NONE',  ( -14.00000000202540029, 1.899127378930379972, 8.000000000004439116 ) ) ;
#15793=VERTEX_POINT ( 'NONE', #8716 ) ;
#15847=AXIS2_PLACEMENT_3D ( 'NONE', #4770, #12035, #17471 ) ;
#15882=ADVANCED_FACE ( 'NONE', ( #15725 ), #10408, .T. ) ;
#15906=VECTOR ( 'NONE', #6325, 1000.000000000000000 ) ;
#15974=DIRECTION ( 'NONE',  ( 1.138590270679734009E-14, 2.220446049251240387E-15, 1.000000000000000000 ) ) ;
#15979=ORIENTED_EDGE ( 'NONE', *, *, #14514, .F. ) ;
#16054=AXIS2_PLACEMENT_3D ( 'NONE', #10592, #17817, #12482 ) ;
#16080=ADVANCED_FACE ( 'NONE', ( #14985 ), #11692, .F. ) ;
#16104=DIRECTION ( 'NONE',  ( 1.138590270679730064E-14, 2.220446049251240387E-15, 1.000000000000000000 ) ) ;
#16127=ORIENTED_EDGE ( 'NONE', *, *, #22588, .T. ) ;
#16153=CYLINDRICAL_SURFACE ( 'NONE', #16838, 2.499999999999998668 ) ;
#16212=CARTESIAN_POINT ( 'NONE',  ( -20.00000000397270128, 22.95208919257349933, 8.000000000004460432 ) ) ;
#16239=ORIENTED_EDGE ( 'NONE', *, *, #11766, .F. ) ;
#16271=ORIENTED_EDGE ( 'NONE', *, *, #11879, .F. ) ;
#16307=CARTESIAN_POINT ( 'NONE',  ( -22.52506282043049879, 26.45208917575140006, 6.750000000004490630 ) ) ;
#16310=AXIS2_PLACEMENT_3D ( 'NONE', #6945, #14174, #5143 ) ;
#16353=DIRECTION ( 'NONE',  ( 1.000000000000000000, 9.248967332749676061E-11, -1.142026288351397951E-14 ) ) ;
#16388=ORIENTED_EDGE ( 'NONE', *, *, #18190, .T. ) ;
#16515=VERTEX_POINT ( 'NONE', #111 ) ;
#16551=LINE ( 'NONE', #46, #22121 ) ;
#16600=EDGE_CURVE ( 'NONE', #15535, #12469, #482, .T. ) ;
#16719=DIRECTION ( 'NONE',  ( -3.332946295912376778E-07, 0.000000000000000000, 0.9999999999999444888 ) ) ;
#16838=AXIS2_PLACEMENT_3D ( 'NONE', #23384, #5347, #1428 ) ;
#16879=CARTESIAN_POINT ( 'NONE',  ( -14.54830929633820169, -2.787889851644860251, 6.750000000004459544 ) ) ;
#16907=PRODUCT_DEFINITION ( 'UNKNOWN', '', #3492, #12095 ) ;
#16918=EDGE_LOOP ( 'NONE', ( #3215, #14609, #3756, #5344 ) ) ;
#16950=ORIENTED_EDGE ( 'NONE', *, *, #4857, .T. ) ;
#16965=VERTEX_POINT ( 'NONE', #10694 ) ;
#17011=CARTESIAN_POINT ( 'NONE',  ( -27.50000000434249969, 26.95208919188020147, 5.500000000004539480 ) ) ;
#17018=CARTESIAN_POINT ( 'NONE',  ( -20.00000000397270128, 22.95208919257349933, 8.000000000004460432 ) ) ;
#17067=EDGE_LOOP ( 'NONE', ( #9310, #4484 ) ) ;
#17073=EDGE_CURVE ( 'NONE', #23388, #6910, #22891, .T. ) ;
#17088=ORIENTED_EDGE ( 'NONE', *, *, #3395, .F. ) ;
#17091=FACE_OUTER_BOUND ( 'NONE', #20280, .T. ) ;
#17126=AXIS2_PLACEMENT_3D ( 'NONE', #9991, #1156, #9859 ) ;
#17156=CARTESIAN_POINT ( 'NONE',  ( -17.47493720815189633, 28.95208920939580111, 8.000000000004419576 ) ) ;
#17219=AXIS2_PLACEMENT_3D ( 'NONE', #17533, #8523, #19311 ) ;
#17234=EDGE_CURVE ( 'NONE', #15046, #1783, #16551, .T. ) ;
#17276=ADVANCED_FACE ( 'NONE', ( #10134 ), #5995, .F. ) ;
#17329=AXIS2_PLACEMENT_3D ( 'NONE', #3070, #1157, #23249 ) ;
#17335=CARTESIAN_POINT ( 'NONE',  ( -17.50000000000000000, -19.99999998334472195, 6.750000000004530598 ) ) ;
#17339=VERTEX_POINT ( 'NONE', #18724 ) ;
#17340=FACE_OUTER_BOUND ( 'NONE', #14870, .T. ) ;
#17372=EDGE_CURVE ( 'NONE', #6910, #10876, #6682, .T. ) ;
#17384=VECTOR ( 'NONE', #11900, 1000.000000000000000 ) ;
#17415=DIRECTION ( 'NONE',  ( 1.138590270679730064E-14, 2.220446049251240387E-15, 1.000000000000000000 ) ) ;
#17435=CARTESIAN_POINT ( 'NONE',  ( -26.00000000397269773, 22.95208919201850151, 8.000000000004529710 ) ) ;
#17441=CARTESIAN_POINT ( 'NONE',  ( -12.50000000434259917, 26.95208919326709918, 8.000000000004369838 ) ) ;
#17471=DIRECTION ( 'NONE',  ( -1.000000000000000000, -6.662111140531837817E-09, 1.110223024625157172E-14 ) ) ;
#17519=ADVANCED_FACE ( 'NONE', ( #3102 ), #16153, .F. ) ;
#17533=CARTESIAN_POINT ( 'NONE',  ( -22.52506282043049879, 26.45208917575140006, 5.500000000004489742 ) ) ;
#17634=CARTESIAN_POINT ( 'NONE',  ( -20.00000000000000000, -20.00000000000000000, 6.750000000004559908 ) ) ;
#17747=CARTESIAN_POINT ( 'NONE',  ( -17.47493720815199936, 28.95208920939580111, 5.500000000004419576 ) ) ;
#17768=FACE_OUTER_BOUND ( 'NONE', #9652, .T. ) ;
#17790=DIRECTION ( 'NONE',  ( -1.000000000000000000, -9.248855984704951398E-11, 1.138590270700269951E-14 ) ) ;
#17794=ADVANCED_FACE ( 'NONE', ( #17091 ), #13646, .F. ) ;
#17817=DIRECTION ( 'NONE',  ( -1.138590270679730064E-14, -2.220446049251235259E-15, -1.000000000000000000 ) ) ;
#17884=ORIENTED_EDGE ( 'NONE', *, *, #11833, .T. ) ;
#17906=AXIS2_PLACEMENT_3D ( 'NONE', #17634, #19523, #10514 ) ;
#17964=ORIENTED_EDGE ( 'NONE', *, *, #17372, .T. ) ;
#17987=CARTESIAN_POINT ( 'NONE',  ( -25.01253141238650102, 26.70208918381559826, 8.000000000004510170 ) ) ;
#18008=CARTESIAN_POINT ( 'NONE',  ( -16.50000000144730095, -4.350228928666989958, 8.000000000004488854 ) ) ;
#18181=ORIENTED_EDGE ( 'NONE', *, *, #22321, .F. ) ;
#18190=EDGE_CURVE ( 'NONE', #3674, #11869, #11175, .T. ) ;
#18249=CARTESIAN_POINT ( 'NONE',  ( -17.47493719149670000, 26.45208920939580111, 8.000000000004430234 ) ) ;
#18364=DIRECTION ( 'NONE',  ( 1.138590270679730064E-14, 2.220446049251235259E-15, 1.000000000000000000 ) ) ;
#18386=ORIENTED_EDGE ( 'NONE', *, *, #7670, .T. ) ;
#18451=CARTESIAN_POINT ( 'NONE',  ( -20.00000000397270128, 22.95208919257349933, 6.750000000004470202 ) ) ;
#18502=CIRCLE ( 'NONE', #2946, 2.500000000000000444 ) ;
#18533=CYLINDRICAL_SURFACE ( 'NONE', #23178, 6.000000000000000000 ) ;
#18537=LINE ( 'NONE', #15074, #1791 ) ;
#18600=ORIENTED_EDGE ( 'NONE', *, *, #21881, .F. ) ;
#18652=DIRECTION ( 'NONE',  ( 1.138590270679731958E-14, 2.220446049251240387E-15, 1.000000000000000000 ) ) ;
#18724=CARTESIAN_POINT ( 'NONE',  ( -25.29411765129259848, 25.77561860384869874, 8.000000000004520828 ) ) ;
#18734=DIRECTION ( 'NONE',  ( 1.000000000000000000, 9.250447630115842075E-11, -1.144917494144692525E-14 ) ) ;
#18759=ORIENTED_EDGE ( 'NONE', *, *, #6028, .T. ) ;
#18821=CIRCLE ( 'NONE', #3999, 2.499999999999998668 ) ;
#18839=ORIENTED_EDGE ( 'NONE', *, *, #17234, .T. ) ;
#18945=CYLINDRICAL_SURFACE ( 'NONE', #14377, 2.500000000000000444 ) ;
#18968=ORIENTED_EDGE ( 'NONE', *, *, #13562, .F. ) ;
#18985=CIRCLE ( 'NONE', #16310, 2.499999999999999112 ) ;
#18996=DIRECTION ( 'NONE',  ( 1.138590270679731958E-14, 2.220446049251245514E-15, 1.000000000000000000 ) ) ;
#19003=ORIENTED_EDGE ( 'NONE', *, *, #2427, .T. ) ;
#19070=CARTESIAN_POINT ( 'NONE',  ( -16.50000000144740042, -4.350228928666989958, 6.750000000004490630 ) ) ;
#19117=DIRECTION ( 'NONE',  ( 0.9949874374308235181, 0.09999999677421511635, -1.144917494144692051E-14 ) ) ;
#19125=AXIS2_PLACEMENT_3D ( 'NONE', #8191, #15421, #10106 ) ;
#19135=ORIENTED_EDGE ( 'NONE', *, *, #11833, .F. ) ;
#19204=FACE_BOUND ( 'NONE', #799, .T. ) ;
#19227=CARTESIAN_POINT ( 'NONE',  ( -14.54830929662709949, 0.3367883020382420045, 6.750000000004450662 ) ) ;
#19255=ORIENTED_EDGE ( 'NONE', *, *, #740, .T. ) ;
#19258=CARTESIAN_POINT ( 'NONE',  ( -22.50000000397270128, 22.95208917591822129, 6.750000000004498624 ) ) ;
#19310=FACE_OUTER_BOUND ( 'NONE', #22788, .T. ) ;
#19311=DIRECTION ( 'NONE',  ( -6.662111140531837817E-09, 1.000000000000000000, -2.081668171172169697E-15 ) ) ;
#19313=DIRECTION ( 'NONE',  ( -1.469367938527859874E-40, 1.000000000000000000, -9.249283497051789705E-11 ) ) ;
#19425=PLANE ( 'NONE',  #6759 ) ;
#19432=ORIENTED_EDGE ( 'NONE', *, *, #22486, .T. ) ;
#19523=DIRECTION ( 'NONE',  ( 1.138590270679730064E-14, 2.220446049251240387E-15, 1.000000000000000000 ) ) ;
#19599=ORIENTED_EDGE ( 'NONE', *, *, #12062, .F. ) ;
#19665=DIRECTION ( 'NONE',  ( 1.138590270679730064E-14, 2.220446049251240387E-15, 1.000000000000000000 ) ) ;
#19671=VERTEX_POINT ( 'NONE', #12500 ) ;
#19727=ORIENTED_EDGE ( 'NONE', *, *, #14344, .T. ) ;
#19735=MECHANICAL_CONTEXT ( 'NONE', #2142, 'mechanical' ) ;
#19755=DIRECTION ( 'NONE',  ( 1.000000000000000000, 6.662111466122900240E-09, -1.138590272159020020E-14 ) ) ;
#19775=CARTESIAN_POINT ( 'NONE',  ( -14.00000000144740042, -4.350228928435730502, 5.500000000004459544 ) ) ;
#19778=DIRECTION ( 'NONE',  ( 1.000000000000000000, 9.248967332749676061E-11, -1.127570259384924611E-14 ) ) ;
#19793=CARTESIAN_POINT ( 'NONE',  ( -20.00000000000000000, -20.00000000000000000, 5.500000000004559020 ) ) ;
#19797=FACE_OUTER_BOUND ( 'NONE', #10666, .T. ) ;
#19812=EDGE_LOOP ( 'NONE', ( #12869, #19135, #12281, #5132 ) ) ;
#19815=CIRCLE ( 'NONE', #21697, 2.499999999999998668 ) ;
#19818=ORIENTED_EDGE ( 'NONE', *, *, #23132, .F. ) ;
#19870=VECTOR ( 'NONE', #5664, 1000.000000000000000 ) ;
#19874=ADVANCED_FACE ( 'NONE', ( #11991 ), #6147, .T. ) ;
#19904=ORIENTED_EDGE ( 'NONE', *, *, #740, .F. ) ;
#19920=PRODUCT ( '1602p_c_17', '1602p_c_17', '', ( #19735 ) ) ;
#19922=AXIS2_PLACEMENT_3D ( 'NONE', #12230, #22763, #19117 ) ;
#20013=CIRCLE ( 'NONE', #15847, 2.499999999999998668 ) ;
#20047=CARTESIAN_POINT ( 'NONE',  ( -26.00000000397269773, 22.95208919201850151, 5.500000000004529710 ) ) ;
#20115=( LENGTH_UNIT ( ) NAMED_UNIT ( * ) SI_UNIT ( .MILLI., .METRE. ) );
#20129=DIRECTION ( 'NONE',  ( -0.8823529412199823119, 0.4705882352125332901, 8.962737959213505425E-15 ) ) ;
#20280=EDGE_LOOP ( 'NONE', ( #10584, #9604, #2738, #7410 ) ) ;
#20335=DIRECTION ( 'NONE',  ( -1.000000000000000000, -6.662111140531837817E-09, 1.144917494144693313E-14 ) ) ;
#20420=CARTESIAN_POINT ( 'NONE',  ( -17.47493720815199936, 28.95208920939580111, 5.500000000004419576 ) ) ;
#20752=EDGE_LOOP ( 'NONE', ( #7039, #7727, #6602, #17088 ) ) ;
#20942=DIRECTION ( 'NONE',  ( 1.138590270679730064E-14, 2.220446049251240387E-15, 1.000000000000000000 ) ) ;
#20983=FACE_BOUND ( 'NONE', #17067, .T. ) ;
#21021=CARTESIAN_POINT ( 'NONE',  ( -20.00479999606049830, 1.846597379377929782, 5.500000000004510170 ) ) ;
#21086=DIRECTION ( 'NONE',  ( -1.138590270679734009E-14, -2.220446049251240387E-15, -1.000000000000000000 ) ) ;
#21174=CARTESIAN_POINT ( 'NONE',  ( -14.98746859791960162, 26.70208920133150343, 6.750000000004400036 ) ) ;
#21199=CARTESIAN_POINT ( 'NONE',  ( -14.00000000397270128, 22.95208919312850071, 6.750000000004400036 ) ) ;
#21203=CARTESIAN_POINT ( 'NONE',  ( -22.50000000397270128, 22.95208917591822129, 8.000000000004487077 ) ) ;
#21329=CARTESIAN_POINT ( 'NONE',  ( -25.01253141238650102, 26.70208918381559826, 6.750000000004510170 ) ) ;
#21446=CARTESIAN_POINT ( 'NONE',  ( -20.00479999606039883, 1.846597379377929782, 8.000000000004510170 ) ) ;
#21447=EDGE_CURVE ( 'NONE', #9763, #1775, #11264, .T. ) ;
#21539=EDGE_CURVE ( 'NONE', #11869, #15046, #7084, .T. ) ;
#21566=DIRECTION ( 'NONE',  ( -9.248855984704951398E-11, 1.000000000000000000, 0.000000000000000000 ) ) ;
#21567=ADVANCED_FACE ( 'NONE', ( #5439 ), #2099, .F. ) ;
#21577=CARTESIAN_POINT ( 'NONE',  ( -17.47493720815199936, 28.95208920939580111, 6.750000000004419576 ) ) ;
#21641=ORIENTED_EDGE ( 'NONE', *, *, #7670, .F. ) ;
#21650=LINE ( 'NONE', #10421, #12799 ) ;
#21697=AXIS2_PLACEMENT_3D ( 'NONE', #13221, #845, #15345 ) ;
#21739=EDGE_CURVE ( 'NONE', #6317, #23250, #666, .T. ) ;
#21873=VERTEX_POINT ( 'NONE', #21203 ) ;
#21881=EDGE_CURVE ( 'NONE', #10063, #11032, #10440, .T. ) ;
#21889=VECTOR ( 'NONE', #514, 1000.000000000000000 ) ;
#21944=ORIENTED_EDGE ( 'NONE', *, *, #23132, .T. ) ;
#21945=DIRECTION ( 'NONE',  ( 1.000000000000000000, 9.248967332749676061E-11, -1.142026288351397951E-14 ) ) ;
#21961=DIRECTION ( 'NONE',  ( 0.7806762821593211665, -0.6249356306643909509, -7.632783294297951215E-15 ) ) ;
#21968=AXIS2_PLACEMENT_3D ( 'NONE', #22258, #4106, #11374 ) ;
#22001=CARTESIAN_POINT ( 'NONE',  ( -22.52506283708579815, 28.95208917575130414, 6.750000000004479972 ) ) ;
#22084=VERTEX_POINT ( 'NONE', #10181 ) ;
#22121=VECTOR ( 'NONE', #16104, 1000.000000000000000 ) ;
#22207=CARTESIAN_POINT ( 'NONE',  ( -17.50000000000000000, -19.99999998334472195, 8.000000000004533263 ) ) ;
#22258=CARTESIAN_POINT ( 'NONE',  ( -20.00000000000000000, -20.00000000000000000, 8.000000000004559908 ) ) ;
#22321=EDGE_CURVE ( 'NONE', #12306, #9811, #21650, .T. ) ;
#22332=LINE ( 'NONE', #16879, #9374 ) ;
#22388=CARTESIAN_POINT ( 'NONE',  ( -14.00000000397270128, 22.95208919312850071, 6.750000000004400036 ) ) ;
#22424=EDGE_LOOP ( 'NONE', ( #107, #18600, #18759, #17884 ) ) ;
#22486=EDGE_CURVE ( 'NONE', #16965, #3768, #14655, .T. ) ;
#22525=CARTESIAN_POINT ( 'NONE',  ( -17.47493719149670000, 26.45208920939580111, 5.500000000004429346 ) ) ;
#22548=ORIENTED_EDGE ( 'NONE', *, *, #11437, .T. ) ;
#22588=EDGE_CURVE ( 'NONE', #3674, #22084, #8131, .T. ) ;
#22658=DIRECTION ( 'NONE',  ( -1.000000000000000000, -6.662111140531837817E-09, 1.144917494144693313E-14 ) ) ;
#22675=CARTESIAN_POINT ( 'NONE',  ( -17.50000000397270128, 22.95208920922877738, 6.750000000004441780 ) ) ;
#22715=EDGE_CURVE ( 'NONE', #23250, #17339, #11321, .T. ) ;
#22757=DIRECTION ( 'NONE',  ( -0.8823529412199823119, 0.4705882352125332901, 8.962737959213505425E-15 ) ) ;
#22763=DIRECTION ( 'NONE',  ( -1.138590270679731958E-14, -2.220446049251245514E-15, -1.000000000000000000 ) ) ;
#22774=ORIENTED_EDGE ( 'NONE', *, *, #15298, .F. ) ;
#22776=AXIS2_PLACEMENT_3D ( 'NONE', #21446, #1131, #8398 ) ;
#22788=EDGE_LOOP ( 'NONE', ( #22548, #18181, #19727, #15281 ) ) ;
#22867=CARTESIAN_POINT ( 'NONE',  ( -14.00000000144740042, -4.350228928435730502, 6.750000000004459544 ) ) ;
#22881=CIRCLE ( 'NONE', #16054, 2.500000000000000444 ) ;
#22891=CIRCLE ( 'NONE', #8103, 5.999999999999999112 ) ;
#22936=ORIENTED_EDGE ( 'NONE', *, *, #21539, .T. ) ;
#22938=CARTESIAN_POINT ( 'NONE',  ( -26.00000000000000000, -20.00000000055539928, 8.000000000004630962 ) ) ;
#23132=EDGE_CURVE ( 'NONE', #15046, #6087, #14614, .T. ) ;
#23178=AXIS2_PLACEMENT_3D ( 'NONE', #2489, #18652, #21945 ) ;
#23249=DIRECTION ( 'NONE',  ( 0.7806762821593211665, -0.6249356306643909509, -7.632783294297951215E-15 ) ) ;
#23250=VERTEX_POINT ( 'NONE', #17435 ) ;
#23294=EDGE_CURVE ( 'NONE', #11032, #3768, #18821, .T. ) ;
#23302=LINE ( 'NONE', #5607, #10145 ) ;
#23322=DIRECTION ( 'NONE',  ( 1.138590270679730064E-14, 2.220446049251240387E-15, 1.000000000000000000 ) ) ;
#23355=CARTESIAN_POINT ( 'NONE',  ( -22.50000000397270128, 22.95208917591822129, 5.500000000004487966 ) ) ;
#23357=ORIENTED_EDGE ( 'NONE', *, *, #13562, .T. ) ;
#23372=ADVANCED_FACE ( 'NONE', ( #19797 ), #9109, .T. ) ;
#23384=CARTESIAN_POINT ( 'NONE',  ( -20.00000000000000000, -20.00000000000000000, 6.750000000004559908 ) ) ;
#23388=VERTEX_POINT ( 'NONE', #10802 ) ;
#23421=CIRCLE ( 'NONE', #2951, 6.000000000000109246 ) ;
#23522=COLOUR_RGB('Light Blue', 0.66274510, 0.83137255, 0.94901961);
#23523=FILL_AREA_STYLE_COLOUR('',#23522);
#23524=FILL_AREA_STYLE('',(#23523));
#23525=SURFACE_STYLE_FILL_AREA(#23524);
#23526=SURFACE_SIDE_STYLE('',(#23525));
#23527=SURFACE_STYLE_USAGE(.BOTH.,#23526);
#23528=PRESENTATION_STYLE_ASSIGNMENT((#23527));
#23591=STYLED_ITEM('',(#23528),#1279);
#23592=MECHANICAL_DESIGN_GEOMETRIC_PRESENTATION_REPRESENTATION('',(#23591),#13514);
ENDSEC;
END-ISO-10303-21;
